ISO-10303-21;
HEADER;
/* Generated by software containing ST-Developer
 * from STEP Tools, Inc. (www.steptools.com) 
 */

FILE_DESCRIPTION(
/* description */ (''),
/* implementation_level */ '2;1');

FILE_NAME(
/* name */ 'Crank_02.step',
/* time_stamp */ '2026-09-20T21:58:27+06:00',
/* author */ (''),
/* organization */ (''),
/* preprocessor_version */ 'ST-DEVELOPER v20.2',
/* originating_system */ 'Autodesk Translation Framework v15.15.0.0',
/* authorisation */ '');

FILE_SCHEMA (('AUTOMOTIVE_DESIGN { 1 0 10303 214 3 1 1 }'));
ENDSEC;

DATA;
#10=MECHANICAL_DESIGN_GEOMETRIC_PRESENTATION_REPRESENTATION('',(#64),#2238);
#48=SHAPE_REPRESENTATION_RELATIONSHIP('SRR','None',#2275,#56);
#56=ADVANCED_BREP_SHAPE_REPRESENTATION('',(#72),#2235);
#64=STYLED_ITEM('',(#2320),#72);
#72=MANIFOLD_SOLID_BREP('Crank_02',#1211);
#81=FACE_BOUND('',#253,.T.);
#82=FACE_BOUND('',#254,.T.);
#83=FACE_BOUND('',#256,.T.);
#84=FACE_BOUND('',#257,.T.);
#111=PLANE('',#1434);
#112=PLANE('',#1435);
#174=FACE_OUTER_BOUND('',#249,.T.);
#175=FACE_OUTER_BOUND('',#250,.T.);
#176=FACE_OUTER_BOUND('',#251,.T.);
#177=FACE_OUTER_BOUND('',#252,.T.);
#178=FACE_OUTER_BOUND('',#255,.T.);
#249=EDGE_LOOP('',(#1040,#1041,#1042,#1043));
#250=EDGE_LOOP('',(#1044,#1045,#1046,#1047));
#251=EDGE_LOOP('',(#1048,#1049,#1050,#1051));
#252=EDGE_LOOP('',(#1052));
#253=EDGE_LOOP('',(#1053));
#254=EDGE_LOOP('',(#1054));
#255=EDGE_LOOP('',(#1055));
#256=EDGE_LOOP('',(#1056));
#257=EDGE_LOOP('',(#1057));
#340=LINE('',#2147,#425);
#341=LINE('',#2153,#426);
#342=LINE('',#2159,#427);
#425=VECTOR('',#1778,13.);
#426=VECTOR('',#1785,2.25);
#427=VECTOR('',#1792,24.1717785126239);
#505=CIRCLE('',#1426,13.);
#506=CIRCLE('',#1427,13.);
#507=CIRCLE('',#1429,2.25);
#508=CIRCLE('',#1430,2.25);
#509=CIRCLE('',#1432,24.1717785126239);
#510=CIRCLE('',#1433,24.1717785126239);
#603=VERTEX_POINT('',#2144);
#604=VERTEX_POINT('',#2146);
#605=VERTEX_POINT('',#2150);
#606=VERTEX_POINT('',#2152);
#607=VERTEX_POINT('',#2156);
#608=VERTEX_POINT('',#2158);
#752=EDGE_CURVE('',#603,#603,#505,.T.);
#753=EDGE_CURVE('',#603,#604,#340,.T.);
#754=EDGE_CURVE('',#604,#604,#506,.T.);
#755=EDGE_CURVE('',#605,#605,#507,.T.);
#756=EDGE_CURVE('',#605,#606,#341,.T.);
#757=EDGE_CURVE('',#606,#606,#508,.T.);
#758=EDGE_CURVE('',#607,#607,#509,.T.);
#759=EDGE_CURVE('',#607,#608,#342,.T.);
#760=EDGE_CURVE('',#608,#608,#510,.T.);
#1040=ORIENTED_EDGE('',*,*,#752,.F.);
#1041=ORIENTED_EDGE('',*,*,#753,.T.);
#1042=ORIENTED_EDGE('',*,*,#754,.F.);
#1043=ORIENTED_EDGE('',*,*,#753,.F.);
#1044=ORIENTED_EDGE('',*,*,#755,.F.);
#1045=ORIENTED_EDGE('',*,*,#756,.T.);
#1046=ORIENTED_EDGE('',*,*,#757,.F.);
#1047=ORIENTED_EDGE('',*,*,#756,.F.);
#1048=ORIENTED_EDGE('',*,*,#758,.F.);
#1049=ORIENTED_EDGE('',*,*,#759,.T.);
#1050=ORIENTED_EDGE('',*,*,#760,.T.);
#1051=ORIENTED_EDGE('',*,*,#759,.F.);
#1052=ORIENTED_EDGE('',*,*,#758,.T.);
#1053=ORIENTED_EDGE('',*,*,#752,.T.);
#1054=ORIENTED_EDGE('',*,*,#755,.T.);
#1055=ORIENTED_EDGE('',*,*,#760,.F.);
#1056=ORIENTED_EDGE('',*,*,#754,.T.);
#1057=ORIENTED_EDGE('',*,*,#757,.T.);
#1131=CYLINDRICAL_SURFACE('',#1425,13.);
#1132=CYLINDRICAL_SURFACE('',#1428,2.25);
#1133=CYLINDRICAL_SURFACE('',#1431,24.1717785126239);
#1190=ADVANCED_FACE('',(#174),#1131,.F.);
#1191=ADVANCED_FACE('',(#175),#1132,.F.);
#1192=ADVANCED_FACE('',(#176),#1133,.T.);
#1193=ADVANCED_FACE('',(#177,#81,#82),#111,.T.);
#1194=ADVANCED_FACE('',(#178,#83,#84),#112,.F.);
#1211=CLOSED_SHELL('',(#1190,#1191,#1192,#1193,#1194));
#1424=AXIS2_PLACEMENT_3D('',#2142,#1772,#1773);
#1425=AXIS2_PLACEMENT_3D('',#2143,#1774,#1775);
#1426=AXIS2_PLACEMENT_3D('',#2145,#1776,#1777);
#1427=AXIS2_PLACEMENT_3D('',#2148,#1779,#1780);
#1428=AXIS2_PLACEMENT_3D('',#2149,#1781,#1782);
#1429=AXIS2_PLACEMENT_3D('',#2151,#1783,#1784);
#1430=AXIS2_PLACEMENT_3D('',#2154,#1786,#1787);
#1431=AXIS2_PLACEMENT_3D('',#2155,#1788,#1789);
#1432=AXIS2_PLACEMENT_3D('',#2157,#1790,#1791);
#1433=AXIS2_PLACEMENT_3D('',#2160,#1793,#1794);
#1434=AXIS2_PLACEMENT_3D('',#2161,#1795,#1796);
#1435=AXIS2_PLACEMENT_3D('',#2162,#1797,#1798);
#1772=DIRECTION('axis',(0.,0.,1.));
#1773=DIRECTION('refdir',(1.,0.,0.));
#1774=DIRECTION('center_axis',(0.,-1.,0.));
#1775=DIRECTION('ref_axis',(1.,0.,0.));
#1776=DIRECTION('center_axis',(0.,-1.,0.));
#1777=DIRECTION('ref_axis',(1.,0.,0.));
#1778=DIRECTION('',(0.,-1.,0.));
#1779=DIRECTION('center_axis',(0.,1.,0.));
#1780=DIRECTION('ref_axis',(1.,0.,0.));
#1781=DIRECTION('center_axis',(0.,-1.,0.));
#1782=DIRECTION('ref_axis',(1.,0.,0.));
#1783=DIRECTION('center_axis',(0.,-1.,0.));
#1784=DIRECTION('ref_axis',(1.,0.,0.));
#1785=DIRECTION('',(0.,-1.,0.));
#1786=DIRECTION('center_axis',(0.,1.,0.));
#1787=DIRECTION('ref_axis',(1.,0.,0.));
#1788=DIRECTION('center_axis',(0.,1.,0.));
#1789=DIRECTION('ref_axis',(1.,0.,0.));
#1790=DIRECTION('center_axis',(0.,1.,0.));
#1791=DIRECTION('ref_axis',(1.,0.,0.));
#1792=DIRECTION('',(0.,-1.,0.));
#1793=DIRECTION('center_axis',(0.,1.,0.));
#1794=DIRECTION('ref_axis',(1.,0.,0.));
#1795=DIRECTION('center_axis',(0.,1.,0.));
#1796=DIRECTION('ref_axis',(1.,0.,0.));
#1797=DIRECTION('center_axis',(0.,1.,0.));
#1798=DIRECTION('ref_axis',(1.,0.,0.));
#2142=CARTESIAN_POINT('',(0.,0.,0.));
#2143=CARTESIAN_POINT('Origin',(0.,0.,24.1717785126239));
#2144=CARTESIAN_POINT('',(-13.,3.,24.1717785126239));
#2145=CARTESIAN_POINT('Origin',(0.,3.,24.1717785126239));
#2146=CARTESIAN_POINT('',(-13.,0.,24.1717785126239));
#2147=CARTESIAN_POINT('',(-13.,0.,24.1717785126239));
#2148=CARTESIAN_POINT('Origin',(0.,0.,24.1717785126239));
#2149=CARTESIAN_POINT('Origin',(-17.3702842355308,0.,34.2005167919079));
#2150=CARTESIAN_POINT('',(-19.6202842355308,3.,34.2005167919079));
#2151=CARTESIAN_POINT('Origin',(-17.3702842355308,3.,34.2005167919079));
#2152=CARTESIAN_POINT('',(-19.6202842355308,0.,34.2005167919079));
#2153=CARTESIAN_POINT('',(-19.6202842355308,0.,34.2005167919079));
#2154=CARTESIAN_POINT('Origin',(-17.3702842355308,0.,34.2005167919079));
#2155=CARTESIAN_POINT('Origin',(0.,0.,24.1717785126239));
#2156=CARTESIAN_POINT('',(-24.1717785126239,3.,24.1717785126239));
#2157=CARTESIAN_POINT('Origin',(0.,3.,24.1717785126239));
#2158=CARTESIAN_POINT('',(-24.1717785126239,0.,24.1717785126239));
#2159=CARTESIAN_POINT('',(-24.1717785126239,0.,24.1717785126239));
#2160=CARTESIAN_POINT('Origin',(0.,0.,24.1717785126239));
#2161=CARTESIAN_POINT('Origin',(0.,3.,24.1717785126239));
#2162=CARTESIAN_POINT('Origin',(0.,0.,24.1717785126239));
#2225=UNCERTAINTY_MEASURE_WITH_UNIT(LENGTH_MEASURE(0.01),#2239,
'DISTANCE_ACCURACY_VALUE',
'Maximum model space distance between geometric entities at asserted c
onnectivities');
#2228=UNCERTAINTY_MEASURE_WITH_UNIT(LENGTH_MEASURE(0.01),#2239,
'DISTANCE_ACCURACY_VALUE',
'Maximum model space distance between geometric entities at asserted c
onnectivities');
#2235=(
GEOMETRIC_REPRESENTATION_CONTEXT(3)
GLOBAL_UNCERTAINTY_ASSIGNED_CONTEXT((#2225))
GLOBAL_UNIT_ASSIGNED_CONTEXT((#2239,#2241,#2242))
REPRESENTATION_CONTEXT('','3D')
);
#2238=(
GEOMETRIC_REPRESENTATION_CONTEXT(3)
GLOBAL_UNCERTAINTY_ASSIGNED_CONTEXT((#2228))
GLOBAL_UNIT_ASSIGNED_CONTEXT((#2239,#2241,#2242))
REPRESENTATION_CONTEXT('','3D')
);
#2239=(
LENGTH_UNIT()
NAMED_UNIT(*)
SI_UNIT(.MILLI.,.METRE.)
);
#2241=(
NAMED_UNIT(*)
PLANE_ANGLE_UNIT()
SI_UNIT($,.RADIAN.)
);
#2242=(
NAMED_UNIT(*)
SI_UNIT($,.STERADIAN.)
SOLID_ANGLE_UNIT()
);
#2249=SHAPE_DEFINITION_REPRESENTATION(#2258,#2275);
#2258=PRODUCT_DEFINITION_SHAPE('',$,#2285);
#2275=SHAPE_REPRESENTATION('',(#1424),#2235);
#2278=PRODUCT_DEFINITION_CONTEXT('part definition',#2307,'design');
#2285=PRODUCT_DEFINITION('Crank_02','Crank_02',#2294,#2278);
#2294=PRODUCT_DEFINITION_FORMATION('',$,#2315);
#2307=APPLICATION_CONTEXT(
'Core Data for Automotive Mechanical Design Process');
#2308=PRODUCT_CONTEXT('part definition',#2307,'mechanical');
#2315=PRODUCT('Crank_02','Crank_02',$,(#2308));
#2320=PRESENTATION_STYLE_ASSIGNMENT((#2324));
#2324=SURFACE_STYLE_USAGE(.BOTH.,#2328);
#2328=SURFACE_SIDE_STYLE('',(#2332));
#2332=SURFACE_STYLE_FILL_AREA(#2336);
#2336=FILL_AREA_STYLE('Surface - Matte',(#2340));
#2340=FILL_AREA_STYLE_COLOUR('Surface - Matte',#2344);
#2344=COLOUR_RGB('Surface - Matte', 0.66274510, 0.83137255, 0.94901961);
ENDSEC;
END-ISO-10303-21;
